ISO-10303-21;
HEADER;
/* Generated by software containing ST-Developer
 * from STEP Tools, Inc. (www.steptools.com) 
 */

FILE_DESCRIPTION(
/* description */ ('Cable chain and bracket set'),
/* implementation_level */ '2;1');

FILE_NAME(
/* name */ 'Forty millimetre hinge bolt.step',
/* time_stamp */ '2026-10-29T17:19:47-07:00',
/* author */ (''),
/* organization */ (''),
/* preprocessor_version */ 'ST-DEVELOPER v20.2',
/* originating_system */ 'Autodesk Translation Framework v15.17.0.0',
/* authorisation */ '');

FILE_SCHEMA (('AUTOMOTIVE_DESIGN { 1 0 10303 214 3 1 1 }'));
ENDSEC;

DATA;
#10=MECHANICAL_DESIGN_GEOMETRIC_PRESENTATION_REPRESENTATION('',(#347),#5929);
#265=(
BOUNDED_CURVE()
B_SPLINE_CURVE(2,(#5690,#5691,#5692),.UNSPECIFIED.,.F.,.F.)
B_SPLINE_CURVE_WITH_KNOTS((3,3),(0.144988513094728,0.791574906712449),
 .UNSPECIFIED.)
CURVE()
GEOMETRIC_REPRESENTATION_ITEM()
RATIONAL_B_SPLINE_CURVE((1.09282032302755,1.26188021535082,1.09282032302931))
REPRESENTATION_ITEM('')
);
#266=(
BOUNDED_CURVE()
B_SPLINE_CURVE(2,(#5694,#5695,#5696),.UNSPECIFIED.,.F.,.F.)
B_SPLINE_CURVE_WITH_KNOTS((3,3),(0.144988513094728,0.791574906712449),
 .UNSPECIFIED.)
CURVE()
GEOMETRIC_REPRESENTATION_ITEM()
RATIONAL_B_SPLINE_CURVE((1.09282032302755,1.26188021535082,1.09282032302931))
REPRESENTATION_ITEM('')
);
#267=(
BOUNDED_CURVE()
B_SPLINE_CURVE(2,(#5698,#5699,#5700),.UNSPECIFIED.,.F.,.F.)
B_SPLINE_CURVE_WITH_KNOTS((3,3),(0.144988513094728,0.791574906712449),
 .UNSPECIFIED.)
CURVE()
GEOMETRIC_REPRESENTATION_ITEM()
RATIONAL_B_SPLINE_CURVE((1.09282032302755,1.26188021535082,1.09282032302931))
REPRESENTATION_ITEM('')
);
#268=(
BOUNDED_CURVE()
B_SPLINE_CURVE(2,(#5702,#5703,#5704),.UNSPECIFIED.,.F.,.F.)
B_SPLINE_CURVE_WITH_KNOTS((3,3),(0.144988513094728,0.791574906712449),
 .UNSPECIFIED.)
CURVE()
GEOMETRIC_REPRESENTATION_ITEM()
RATIONAL_B_SPLINE_CURVE((1.09282032302755,1.26188021535082,1.09282032302931))
REPRESENTATION_ITEM('')
);
#269=(
BOUNDED_CURVE()
B_SPLINE_CURVE(2,(#5706,#5707,#5708),.UNSPECIFIED.,.F.,.F.)
B_SPLINE_CURVE_WITH_KNOTS((3,3),(0.144988513094728,0.791574906712449),
 .UNSPECIFIED.)
CURVE()
GEOMETRIC_REPRESENTATION_ITEM()
RATIONAL_B_SPLINE_CURVE((1.09282032302755,1.26188021535082,1.09282032302931))
REPRESENTATION_ITEM('')
);
#270=(
BOUNDED_CURVE()
B_SPLINE_CURVE(2,(#5709,#5710,#5711),.UNSPECIFIED.,.F.,.F.)
B_SPLINE_CURVE_WITH_KNOTS((3,3),(0.144988513094727,0.791574906712449),
 .UNSPECIFIED.)
CURVE()
GEOMETRIC_REPRESENTATION_ITEM()
RATIONAL_B_SPLINE_CURVE((1.09282032302755,1.26188021535082,1.09282032302931))
REPRESENTATION_ITEM('')
);
#287=CONICAL_SURFACE('',#3726,0.27,0.785398163397448);
#288=CONICAL_SURFACE('',#3727,0.576175134594813,1.0471975511966);
#321=SHAPE_REPRESENTATION_RELATIONSHIP('SRR','None',#6059,#334);
#334=ADVANCED_BREP_SHAPE_REPRESENTATION('',(#360),#5926);
#347=STYLED_ITEM('',(#6227),#360);
#360=MANIFOLD_SOLID_BREP('Body1',#3341);
#399=FACE_BOUND('',#899,.T.);
#400=FACE_BOUND('',#913,.T.);
#507=PLANE('',#3717);
#508=PLANE('',#3722);
#509=PLANE('',#3729);
#510=PLANE('',#3730);
#511=PLANE('',#3731);
#512=PLANE('',#3732);
#513=PLANE('',#3733);
#514=PLANE('',#3734);
#515=PLANE('',#3735);
#516=PLANE('',#3736);
#680=FACE_OUTER_BOUND('',#898,.T.);
#681=FACE_OUTER_BOUND('',#900,.T.);
#682=FACE_OUTER_BOUND('',#901,.T.);
#683=FACE_OUTER_BOUND('',#902,.T.);
#684=FACE_OUTER_BOUND('',#903,.T.);
#685=FACE_OUTER_BOUND('',#904,.T.);
#686=FACE_OUTER_BOUND('',#905,.T.);
#687=FACE_OUTER_BOUND('',#906,.T.);
#688=FACE_OUTER_BOUND('',#907,.T.);
#689=FACE_OUTER_BOUND('',#908,.T.);
#690=FACE_OUTER_BOUND('',#909,.T.);
#691=FACE_OUTER_BOUND('',#910,.T.);
#692=FACE_OUTER_BOUND('',#911,.T.);
#693=FACE_OUTER_BOUND('',#912,.T.);
#898=EDGE_LOOP('',(#2979));
#899=EDGE_LOOP('',(#2980));
#900=EDGE_LOOP('',(#2981,#2982,#2983,#2984));
#901=EDGE_LOOP('',(#2985));
#902=EDGE_LOOP('',(#2986,#2987,#2988,#2989));
#903=EDGE_LOOP('',(#2990,#2991,#2992,#2993));
#904=EDGE_LOOP('',(#2994,#2995,#2996,#2997,#2998,#2999,#3000,#3001,#3002));
#905=EDGE_LOOP('',(#3003,#3004,#3005,#3006));
#906=EDGE_LOOP('',(#3007,#3008,#3009,#3010));
#907=EDGE_LOOP('',(#3011,#3012,#3013,#3014));
#908=EDGE_LOOP('',(#3015,#3016,#3017,#3018));
#909=EDGE_LOOP('',(#3019,#3020,#3021,#3022));
#910=EDGE_LOOP('',(#3023,#3024,#3025,#3026));
#911=EDGE_LOOP('',(#3027));
#912=EDGE_LOOP('',(#3028,#3029,#3030,#3031,#3032,#3033));
#913=EDGE_LOOP('',(#3034));
#1166=LINE('',#5673,#1426);
#1167=LINE('',#5680,#1427);
#1168=LINE('',#5683,#1428);
#1169=LINE('',#5688,#1429);
#1170=LINE('',#5714,#1430);
#1171=LINE('',#5716,#1431);
#1172=LINE('',#5717,#1432);
#1173=LINE('',#5720,#1433);
#1174=LINE('',#5721,#1434);
#1175=LINE('',#5724,#1435);
#1176=LINE('',#5725,#1436);
#1177=LINE('',#5728,#1437);
#1178=LINE('',#5729,#1438);
#1179=LINE('',#5732,#1439);
#1180=LINE('',#5733,#1440);
#1181=LINE('',#5735,#1441);
#1426=VECTOR('',#4645,0.3);
#1427=VECTOR('',#4654,0.3);
#1428=VECTOR('',#4659,0.27);
#1429=VECTOR('',#4664,0.576175134594813);
#1430=VECTOR('',#4667,1.);
#1431=VECTOR('',#4668,1.);
#1432=VECTOR('',#4669,1.);
#1433=VECTOR('',#4672,1.);
#1434=VECTOR('',#4673,1.);
#1435=VECTOR('',#4676,1.);
#1436=VECTOR('',#4677,1.);
#1437=VECTOR('',#4680,1.);
#1438=VECTOR('',#4681,1.);
#1439=VECTOR('',#4684,1.);
#1440=VECTOR('',#4685,1.);
#1441=VECTOR('',#4688,1.);
#1547=CIRCLE('',#3718,0.3);
#1548=CIRCLE('',#3719,0.25);
#1549=CIRCLE('',#3721,0.3);
#1550=CIRCLE('',#3724,0.2942);
#1551=CIRCLE('',#3725,0.2942);
#1552=CIRCLE('',#3728,0.475);
#1787=VERTEX_POINT('',#5667);
#1788=VERTEX_POINT('',#5669);
#1789=VERTEX_POINT('',#5672);
#1790=VERTEX_POINT('',#5677);
#1791=VERTEX_POINT('',#5679);
#1792=VERTEX_POINT('',#5685);
#1793=VERTEX_POINT('',#5687);
#1794=VERTEX_POINT('',#5689);
#1795=VERTEX_POINT('',#5693);
#1796=VERTEX_POINT('',#5697);
#1797=VERTEX_POINT('',#5701);
#1798=VERTEX_POINT('',#5705);
#1799=VERTEX_POINT('',#5713);
#1800=VERTEX_POINT('',#5715);
#1801=VERTEX_POINT('',#5719);
#1802=VERTEX_POINT('',#5723);
#1803=VERTEX_POINT('',#5727);
#1804=VERTEX_POINT('',#5731);
#2190=EDGE_CURVE('',#1787,#1787,#1547,.T.);
#2191=EDGE_CURVE('',#1788,#1788,#1548,.T.);
#2192=EDGE_CURVE('',#1787,#1789,#1166,.T.);
#2193=EDGE_CURVE('',#1789,#1789,#1549,.T.);
#2194=EDGE_CURVE('',#1790,#1790,#1550,.F.);
#2195=EDGE_CURVE('',#1790,#1791,#1167,.T.);
#2196=EDGE_CURVE('',#1791,#1791,#1551,.F.);
#2197=EDGE_CURVE('',#1788,#1790,#1168,.T.);
#2198=EDGE_CURVE('',#1792,#1792,#1552,.T.);
#2199=EDGE_CURVE('',#1792,#1793,#1169,.T.);
#2200=EDGE_CURVE('',#1794,#1793,#265,.T.);
#2201=EDGE_CURVE('',#1795,#1794,#266,.T.);
#2202=EDGE_CURVE('',#1796,#1795,#267,.T.);
#2203=EDGE_CURVE('',#1797,#1796,#268,.T.);
#2204=EDGE_CURVE('',#1798,#1797,#269,.T.);
#2205=EDGE_CURVE('',#1793,#1798,#270,.T.);
#2206=EDGE_CURVE('',#1799,#1797,#1170,.T.);
#2207=EDGE_CURVE('',#1799,#1800,#1171,.T.);
#2208=EDGE_CURVE('',#1800,#1798,#1172,.T.);
#2209=EDGE_CURVE('',#1801,#1796,#1173,.T.);
#2210=EDGE_CURVE('',#1801,#1799,#1174,.T.);
#2211=EDGE_CURVE('',#1802,#1795,#1175,.T.);
#2212=EDGE_CURVE('',#1802,#1801,#1176,.T.);
#2213=EDGE_CURVE('',#1803,#1794,#1177,.T.);
#2214=EDGE_CURVE('',#1803,#1802,#1178,.T.);
#2215=EDGE_CURVE('',#1804,#1793,#1179,.T.);
#2216=EDGE_CURVE('',#1804,#1803,#1180,.T.);
#2217=EDGE_CURVE('',#1800,#1804,#1181,.T.);
#2979=ORIENTED_EDGE('',*,*,#2190,.T.);
#2980=ORIENTED_EDGE('',*,*,#2191,.F.);
#2981=ORIENTED_EDGE('',*,*,#2190,.F.);
#2982=ORIENTED_EDGE('',*,*,#2192,.T.);
#2983=ORIENTED_EDGE('',*,*,#2193,.T.);
#2984=ORIENTED_EDGE('',*,*,#2192,.F.);
#2985=ORIENTED_EDGE('',*,*,#2193,.F.);
#2986=ORIENTED_EDGE('',*,*,#2194,.F.);
#2987=ORIENTED_EDGE('',*,*,#2195,.T.);
#2988=ORIENTED_EDGE('',*,*,#2196,.F.);
#2989=ORIENTED_EDGE('',*,*,#2195,.F.);
#2990=ORIENTED_EDGE('',*,*,#2191,.T.);
#2991=ORIENTED_EDGE('',*,*,#2197,.T.);
#2992=ORIENTED_EDGE('',*,*,#2194,.T.);
#2993=ORIENTED_EDGE('',*,*,#2197,.F.);
#2994=ORIENTED_EDGE('',*,*,#2198,.F.);
#2995=ORIENTED_EDGE('',*,*,#2199,.T.);
#2996=ORIENTED_EDGE('',*,*,#2200,.F.);
#2997=ORIENTED_EDGE('',*,*,#2201,.F.);
#2998=ORIENTED_EDGE('',*,*,#2202,.F.);
#2999=ORIENTED_EDGE('',*,*,#2203,.F.);
#3000=ORIENTED_EDGE('',*,*,#2204,.F.);
#3001=ORIENTED_EDGE('',*,*,#2205,.F.);
#3002=ORIENTED_EDGE('',*,*,#2199,.F.);
#3003=ORIENTED_EDGE('',*,*,#2204,.T.);
#3004=ORIENTED_EDGE('',*,*,#2206,.F.);
#3005=ORIENTED_EDGE('',*,*,#2207,.T.);
#3006=ORIENTED_EDGE('',*,*,#2208,.T.);
#3007=ORIENTED_EDGE('',*,*,#2203,.T.);
#3008=ORIENTED_EDGE('',*,*,#2209,.F.);
#3009=ORIENTED_EDGE('',*,*,#2210,.T.);
#3010=ORIENTED_EDGE('',*,*,#2206,.T.);
#3011=ORIENTED_EDGE('',*,*,#2202,.T.);
#3012=ORIENTED_EDGE('',*,*,#2211,.F.);
#3013=ORIENTED_EDGE('',*,*,#2212,.T.);
#3014=ORIENTED_EDGE('',*,*,#2209,.T.);
#3015=ORIENTED_EDGE('',*,*,#2201,.T.);
#3016=ORIENTED_EDGE('',*,*,#2213,.F.);
#3017=ORIENTED_EDGE('',*,*,#2214,.T.);
#3018=ORIENTED_EDGE('',*,*,#2211,.T.);
#3019=ORIENTED_EDGE('',*,*,#2200,.T.);
#3020=ORIENTED_EDGE('',*,*,#2215,.F.);
#3021=ORIENTED_EDGE('',*,*,#2216,.T.);
#3022=ORIENTED_EDGE('',*,*,#2213,.T.);
#3023=ORIENTED_EDGE('',*,*,#2205,.T.);
#3024=ORIENTED_EDGE('',*,*,#2208,.F.);
#3025=ORIENTED_EDGE('',*,*,#2217,.T.);
#3026=ORIENTED_EDGE('',*,*,#2215,.T.);
#3027=ORIENTED_EDGE('',*,*,#2198,.T.);
#3028=ORIENTED_EDGE('',*,*,#2212,.F.);
#3029=ORIENTED_EDGE('',*,*,#2214,.F.);
#3030=ORIENTED_EDGE('',*,*,#2216,.F.);
#3031=ORIENTED_EDGE('',*,*,#2217,.F.);
#3032=ORIENTED_EDGE('',*,*,#2207,.F.);
#3033=ORIENTED_EDGE('',*,*,#2210,.F.);
#3034=ORIENTED_EDGE('',*,*,#2196,.T.);
#3144=CYLINDRICAL_SURFACE('',#3720,0.3);
#3145=CYLINDRICAL_SURFACE('',#3723,0.2942);
#3302=ADVANCED_FACE('',(#680,#399),#507,.T.);
#3303=ADVANCED_FACE('',(#681),#3144,.T.);
#3304=ADVANCED_FACE('',(#682),#508,.F.);
#3305=ADVANCED_FACE('',(#683),#3145,.T.);
#3306=ADVANCED_FACE('',(#684),#287,.T.);
#3307=ADVANCED_FACE('',(#685),#288,.T.);
#3308=ADVANCED_FACE('',(#686),#509,.T.);
#3309=ADVANCED_FACE('',(#687),#510,.T.);
#3310=ADVANCED_FACE('',(#688),#511,.T.);
#3311=ADVANCED_FACE('',(#689),#512,.T.);
#3312=ADVANCED_FACE('',(#690),#513,.T.);
#3313=ADVANCED_FACE('',(#691),#514,.T.);
#3314=ADVANCED_FACE('',(#692),#515,.T.);
#3315=ADVANCED_FACE('',(#693,#400),#516,.F.);
#3341=CLOSED_SHELL('',(#3302,#3303,#3304,#3305,#3306,#3307,#3308,#3309,
#3310,#3311,#3312,#3313,#3314,#3315));
#3716=AXIS2_PLACEMENT_3D('',#5665,#4635,#4636);
#3717=AXIS2_PLACEMENT_3D('',#5666,#4637,#4638);
#3718=AXIS2_PLACEMENT_3D('',#5668,#4639,#4640);
#3719=AXIS2_PLACEMENT_3D('',#5670,#4641,#4642);
#3720=AXIS2_PLACEMENT_3D('',#5671,#4643,#4644);
#3721=AXIS2_PLACEMENT_3D('',#5674,#4646,#4647);
#3722=AXIS2_PLACEMENT_3D('',#5675,#4648,#4649);
#3723=AXIS2_PLACEMENT_3D('',#5676,#4650,#4651);
#3724=AXIS2_PLACEMENT_3D('',#5678,#4652,#4653);
#3725=AXIS2_PLACEMENT_3D('',#5681,#4655,#4656);
#3726=AXIS2_PLACEMENT_3D('',#5682,#4657,#4658);
#3727=AXIS2_PLACEMENT_3D('',#5684,#4660,#4661);
#3728=AXIS2_PLACEMENT_3D('',#5686,#4662,#4663);
#3729=AXIS2_PLACEMENT_3D('',#5712,#4665,#4666);
#3730=AXIS2_PLACEMENT_3D('',#5718,#4670,#4671);
#3731=AXIS2_PLACEMENT_3D('',#5722,#4674,#4675);
#3732=AXIS2_PLACEMENT_3D('',#5726,#4678,#4679);
#3733=AXIS2_PLACEMENT_3D('',#5730,#4682,#4683);
#3734=AXIS2_PLACEMENT_3D('',#5734,#4686,#4687);
#3735=AXIS2_PLACEMENT_3D('',#5736,#4689,#4690);
#3736=AXIS2_PLACEMENT_3D('',#5737,#4691,#4692);
#4635=DIRECTION('axis',(0.,0.,1.));
#4636=DIRECTION('refdir',(1.,0.,0.));
#4637=DIRECTION('center_axis',(0.,1.,0.));
#4638=DIRECTION('ref_axis',(1.,0.,0.));
#4639=DIRECTION('center_axis',(0.,1.,0.));
#4640=DIRECTION('ref_axis',(1.,0.,0.));
#4641=DIRECTION('center_axis',(0.,1.,0.));
#4642=DIRECTION('ref_axis',(1.,0.,0.));
#4643=DIRECTION('center_axis',(0.,1.,0.));
#4644=DIRECTION('ref_axis',(1.,0.,0.));
#4645=DIRECTION('',(0.,-1.,0.));
#4646=DIRECTION('center_axis',(0.,1.,0.));
#4647=DIRECTION('ref_axis',(1.,0.,0.));
#4648=DIRECTION('center_axis',(0.,1.,0.));
#4649=DIRECTION('ref_axis',(1.,0.,0.));
#4650=DIRECTION('center_axis',(0.,-1.,0.));
#4651=DIRECTION('ref_axis',(1.,0.,0.));
#4652=DIRECTION('center_axis',(0.,1.,0.));
#4653=DIRECTION('ref_axis',(1.,0.,0.));
#4654=DIRECTION('',(0.,1.,0.));
#4655=DIRECTION('center_axis',(0.,-1.,0.));
#4656=DIRECTION('ref_axis',(1.,0.,0.));
#4657=DIRECTION('center_axis',(0.,1.,0.));
#4658=DIRECTION('ref_axis',(1.,0.,0.));
#4659=DIRECTION('',(-0.707106781186547,0.707106781186548,-8.65956056235493E-17));
#4660=DIRECTION('center_axis',(0.,-1.,0.));
#4661=DIRECTION('ref_axis',(1.,0.,0.));
#4662=DIRECTION('center_axis',(0.,1.,0.));
#4663=DIRECTION('ref_axis',(1.,0.,0.));
#4664=DIRECTION('',(-0.866025403784439,-0.5,-1.06057523872491E-16));
#4665=DIRECTION('center_axis',(1.92296268638356E-16,0.,-1.));
#4666=DIRECTION('ref_axis',(-1.,0.,-1.92296268638356E-16));
#4667=DIRECTION('',(0.,1.,0.));
#4668=DIRECTION('',(-1.,0.,-1.92296268638356E-16));
#4669=DIRECTION('',(0.,1.,0.));
#4670=DIRECTION('center_axis',(0.866025403784439,0.,-0.5));
#4671=DIRECTION('ref_axis',(-0.5,0.,-0.866025403784439));
#4672=DIRECTION('',(0.,1.,0.));
#4673=DIRECTION('',(-0.5,0.,-0.866025403784439));
#4674=DIRECTION('center_axis',(0.866025403784439,0.,0.5));
#4675=DIRECTION('ref_axis',(0.5,0.,-0.866025403784439));
#4676=DIRECTION('',(0.,1.,0.));
#4677=DIRECTION('',(0.5,0.,-0.866025403784439));
#4678=DIRECTION('center_axis',(-1.92296268638356E-16,0.,1.));
#4679=DIRECTION('ref_axis',(1.,0.,1.92296268638356E-16));
#4680=DIRECTION('',(0.,1.,0.));
#4681=DIRECTION('',(1.,0.,1.92296268638356E-16));
#4682=DIRECTION('center_axis',(-0.866025403784439,0.,0.5));
#4683=DIRECTION('ref_axis',(0.5,0.,0.866025403784439));
#4684=DIRECTION('',(0.,1.,0.));
#4685=DIRECTION('',(0.5,0.,0.866025403784439));
#4686=DIRECTION('center_axis',(-0.866025403784439,0.,-0.5));
#4687=DIRECTION('ref_axis',(-0.5,0.,0.866025403784439));
#4688=DIRECTION('',(-0.5,0.,0.866025403784438));
#4689=DIRECTION('center_axis',(0.,1.,0.));
#4690=DIRECTION('ref_axis',(0.,0.,1.));
#4691=DIRECTION('center_axis',(0.,1.,0.));
#4692=DIRECTION('ref_axis',(1.,0.,0.));
#5665=CARTESIAN_POINT('',(0.,0.,0.));
#5666=CARTESIAN_POINT('Origin',(0.,-2.99,0.));
#5667=CARTESIAN_POINT('',(-0.3,-2.99,3.67394039744206E-17));
#5668=CARTESIAN_POINT('Origin',(0.,-2.99,0.));
#5669=CARTESIAN_POINT('',(-0.25,-2.99,3.06161699786838E-17));
#5670=CARTESIAN_POINT('Origin',(0.,-2.99,0.));
#5671=CARTESIAN_POINT('Origin',(0.,-4.,0.));
#5672=CARTESIAN_POINT('',(-0.3,-4.,3.67394039744206E-17));
#5673=CARTESIAN_POINT('',(-0.3,-4.,3.67394039744206E-17));
#5674=CARTESIAN_POINT('Origin',(0.,-4.,0.));
#5675=CARTESIAN_POINT('Origin',(0.,-4.,0.));
#5676=CARTESIAN_POINT('Origin',(0.,-1.445,0.));
#5677=CARTESIAN_POINT('',(-0.2942,-2.9458,3.60291088309151E-17));
#5678=CARTESIAN_POINT('Origin',(0.,-2.9458,0.));
#5679=CARTESIAN_POINT('',(-0.2942,0.,-3.60291088309151E-17));
#5680=CARTESIAN_POINT('',(-0.2942,-1.445,-3.60291088309151E-17));
#5681=CARTESIAN_POINT('Origin',(0.,0.,0.));
#5682=CARTESIAN_POINT('Origin',(0.,-2.97,0.));
#5683=CARTESIAN_POINT('',(-0.27,-2.97,-3.30654635769785E-17));
#5684=CARTESIAN_POINT('Origin',(0.,0.341586508806388,0.));
#5685=CARTESIAN_POINT('',(-0.475,0.4,-5.81707229594993E-17));
#5686=CARTESIAN_POINT('Origin',(0.,0.4,0.));
#5687=CARTESIAN_POINT('',(-0.577350269189626,0.340908044531739,-7.07050159149938E-17));
#5688=CARTESIAN_POINT('',(-0.576175134594813,0.341586508806388,-7.05611034329833E-17));
#5689=CARTESIAN_POINT('',(-0.288675134594813,0.340908044531739,0.5));
#5690=CARTESIAN_POINT('Ctrl Pts',(-0.288675134594813,0.340908044531739,
0.5));
#5691=CARTESIAN_POINT('Ctrl Pts',(-0.433012701893303,0.424241377863696,
0.249999999998124));
#5692=CARTESIAN_POINT('Ctrl Pts',(-0.577350269189626,0.340908044531739,
-7.07050159149938E-17));
#5693=CARTESIAN_POINT('',(0.288675134594813,0.340908044531739,0.5));
#5694=CARTESIAN_POINT('Ctrl Pts',(0.288675134594813,0.340908044531739,0.5));
#5695=CARTESIAN_POINT('Ctrl Pts',(-2.16648921025353E-12,0.424241377863696,
0.5));
#5696=CARTESIAN_POINT('Ctrl Pts',(-0.288675134594813,0.340908044531739,
0.5));
#5697=CARTESIAN_POINT('',(0.577350269189626,0.340908044531739,0.));
#5698=CARTESIAN_POINT('Ctrl Pts',(0.577350269189626,0.340908044531739,0.));
#5699=CARTESIAN_POINT('Ctrl Pts',(0.433012701891136,0.424241377863697,0.250000000001876));
#5700=CARTESIAN_POINT('Ctrl Pts',(0.288675134594813,0.340908044531739,0.5));
#5701=CARTESIAN_POINT('',(0.288675134594813,0.340908044531739,-0.5));
#5702=CARTESIAN_POINT('Ctrl Pts',(0.288675134594813,0.340908044531739,-0.5));
#5703=CARTESIAN_POINT('Ctrl Pts',(0.433012701893303,0.424241377863696,-0.249999999998124));
#5704=CARTESIAN_POINT('Ctrl Pts',(0.577350269189626,0.340908044531739,0.));
#5705=CARTESIAN_POINT('',(-0.288675134594813,0.340908044531739,-0.5));
#5706=CARTESIAN_POINT('Ctrl Pts',(-0.288675134594813,0.340908044531739,
-0.5));
#5707=CARTESIAN_POINT('Ctrl Pts',(2.16660023255599E-12,0.424241377863696,
-0.5));
#5708=CARTESIAN_POINT('Ctrl Pts',(0.288675134594813,0.340908044531739,-0.5));
#5709=CARTESIAN_POINT('Ctrl Pts',(-0.577350269189626,0.340908044531739,
-7.07050159149938E-17));
#5710=CARTESIAN_POINT('Ctrl Pts',(-0.433012701891136,0.424241377863697,
-0.250000000001876));
#5711=CARTESIAN_POINT('Ctrl Pts',(-0.288675134594813,0.340908044531739,
-0.5));
#5712=CARTESIAN_POINT('Origin',(0.288675134594813,0.,-0.5));
#5713=CARTESIAN_POINT('',(0.288675134594813,0.,-0.5));
#5714=CARTESIAN_POINT('',(0.288675134594813,0.,-0.5));
#5715=CARTESIAN_POINT('',(-0.288675134594813,0.,-0.5));
#5716=CARTESIAN_POINT('',(0.288675134594813,0.,-0.5));
#5717=CARTESIAN_POINT('',(-0.288675134594813,0.,-0.5));
#5718=CARTESIAN_POINT('Origin',(0.577350269189626,0.,0.));
#5719=CARTESIAN_POINT('',(0.577350269189626,0.,0.));
#5720=CARTESIAN_POINT('',(0.577350269189626,0.,0.));
#5721=CARTESIAN_POINT('',(0.577350269189626,0.,0.));
#5722=CARTESIAN_POINT('Origin',(0.288675134594813,0.,0.5));
#5723=CARTESIAN_POINT('',(0.288675134594813,0.,0.5));
#5724=CARTESIAN_POINT('',(0.288675134594813,0.,0.5));
#5725=CARTESIAN_POINT('',(0.288675134594813,0.,0.5));
#5726=CARTESIAN_POINT('Origin',(-0.288675134594813,0.,0.5));
#5727=CARTESIAN_POINT('',(-0.288675134594813,0.,0.5));
#5728=CARTESIAN_POINT('',(-0.288675134594813,0.,0.5));
#5729=CARTESIAN_POINT('',(-0.288675134594813,0.,0.5));
#5730=CARTESIAN_POINT('Origin',(-0.577350269189626,0.,-7.07050159149938E-17));
#5731=CARTESIAN_POINT('',(-0.577350269189626,0.,-7.07050159149938E-17));
#5732=CARTESIAN_POINT('',(-0.577350269189626,0.,-7.07050159149938E-17));
#5733=CARTESIAN_POINT('',(-0.577350269189626,0.,-7.07050159149938E-17));
#5734=CARTESIAN_POINT('Origin',(-0.288675134594813,0.,-0.5));
#5735=CARTESIAN_POINT('',(-0.288675134594813,0.,-0.5));
#5736=CARTESIAN_POINT('Origin',(0.,0.4,0.));
#5737=CARTESIAN_POINT('Origin',(0.,0.,0.));
#5902=UNCERTAINTY_MEASURE_WITH_UNIT(LENGTH_MEASURE(0.001),#5930,
'DISTANCE_ACCURACY_VALUE',
'Maximum model space distance between geometric entities at asserted c
onnectivities');
#5905=UNCERTAINTY_MEASURE_WITH_UNIT(LENGTH_MEASURE(0.001),#5930,
'DISTANCE_ACCURACY_VALUE',
'Maximum model space distance between geometric entities at asserted c
onnectivities');
#5926=(
GEOMETRIC_REPRESENTATION_CONTEXT(3)
GLOBAL_UNCERTAINTY_ASSIGNED_CONTEXT((#5902))
GLOBAL_UNIT_ASSIGNED_CONTEXT((#5930,#5932,#5933))
REPRESENTATION_CONTEXT('','3D')
);
#5929=(
GEOMETRIC_REPRESENTATION_CONTEXT(3)
GLOBAL_UNCERTAINTY_ASSIGNED_CONTEXT((#5905))
GLOBAL_UNIT_ASSIGNED_CONTEXT((#5930,#5932,#5933))
REPRESENTATION_CONTEXT('','3D')
);
#5930=(
LENGTH_UNIT()
NAMED_UNIT(*)
SI_UNIT(.CENTI.,.METRE.)
);
#5932=(
NAMED_UNIT(*)
PLANE_ANGLE_UNIT()
SI_UNIT($,.RADIAN.)
);
#5933=(
NAMED_UNIT(*)
SI_UNIT($,.STERADIAN.)
SOLID_ANGLE_UNIT()
);
#5954=SHAPE_DEFINITION_REPRESENTATION(#5984,#6059);
#5984=PRODUCT_DEFINITION_SHAPE('',$,#6083);
#6059=SHAPE_REPRESENTATION('',(#3716),#5926);
#6062=PRODUCT_DEFINITION_CONTEXT('part definition',#6133,'design');
#6083=PRODUCT_DEFINITION('Forty millimetre hinge bolt',
'Forty millimetre hinge bolt',#6106,#6062);
#6106=PRODUCT_DEFINITION_FORMATION('',$,#6155);
#6133=APPLICATION_CONTEXT(
'Core Data for Automotive Mechanical Design Process');
#6134=PRODUCT_CONTEXT('part definition',#6133,'mechanical');
#6155=PRODUCT('Forty millimetre hinge bolt',
'Forty millimetre hinge bolt','Forty millimetre hinge bolt',(#6134));
#6221=COLOUR_RGB('Black',0.12,0.14,0.17);
#6222=FILL_AREA_STYLE_COLOUR('',#6221);
#6223=FILL_AREA_STYLE('',(#6222));
#6224=SURFACE_STYLE_FILL_AREA(#6223);
#6225=SURFACE_SIDE_STYLE('',(#6224));
#6226=SURFACE_STYLE_USAGE(.BOTH.,#6225);
#6227=PRESENTATION_STYLE_ASSIGNMENT((#6226));
ENDSEC;
END-ISO-10303-21;
